ISO-10303-21;
HEADER;
/* Generated by software containing ST-Developer
 * from STEP Tools, Inc. (www.steptools.com) 
 */

FILE_DESCRIPTION(
/* description */ ('Independent pair of monolithic parallel-leaf compliant finger modules.
 Shared native part/module instances; external gripper actuator outsid
e scope. Whole-mm geometry,1mm webs,56mm straight span,12mm depth,32mm
 nominal contact gap. Undeformed CAD reference; material condition, el
astic range, fatigue and gripping force unassigned.'),
/* implementation_level */ '2;1');

FILE_NAME(
/* name */ 'Flat washer M5.step',
/* time_stamp */ '2026-11-07T22:36:16-08:00',
/* author */ (''),
/* organization */ (''),
/* preprocessor_version */ 'ST-DEVELOPER v20.2',
/* originating_system */ 'Autodesk Translation Framework v15.17.0.0',
/* authorisation */ '');

FILE_SCHEMA (('AUTOMOTIVE_DESIGN { 1 0 10303 214 3 1 1 }'));
ENDSEC;

DATA;
#10=MECHANICAL_DESIGN_GEOMETRIC_PRESENTATION_REPRESENTATION('',(#332),#13801);
#320=SHAPE_REPRESENTATION_RELATIONSHIP('SRR','None',#13838,#326);
#326=ADVANCED_BREP_SHAPE_REPRESENTATION('',(#338),#13798);
#332=STYLED_ITEM('',(#13881),#338);
#338=MANIFOLD_SOLID_BREP('Body1',#3697);
#361=FACE_BOUND('',#759,.T.);
#362=FACE_BOUND('',#761,.T.);
#403=PLANE('',#3939);
#404=PLANE('',#3940);
#535=FACE_OUTER_BOUND('',#756,.T.);
#536=FACE_OUTER_BOUND('',#757,.T.);
#537=FACE_OUTER_BOUND('',#758,.T.);
#538=FACE_OUTER_BOUND('',#760,.T.);
#756=EDGE_LOOP('',(#2901,#2902,#2903,#2904));
#757=EDGE_LOOP('',(#2905,#2906,#2907,#2908));
#758=EDGE_LOOP('',(#2909));
#759=EDGE_LOOP('',(#2910));
#760=EDGE_LOOP('',(#2911));
#761=EDGE_LOOP('',(#2912));
#989=LINE('',#9385,#1218);
#990=LINE('',#9391,#1219);
#1218=VECTOR('',#4522,3.);
#1219=VECTOR('',#4529,6.);
#1347=CIRCLE('',#3934,3.);
#1348=CIRCLE('',#3935,3.);
#1349=CIRCLE('',#3937,6.);
#1350=CIRCLE('',#3938,6.);
#1572=VERTEX_POINT('',#9382);
#1573=VERTEX_POINT('',#9384);
#1574=VERTEX_POINT('',#9388);
#1575=VERTEX_POINT('',#9390);
#2040=EDGE_CURVE('',#1572,#1572,#1347,.T.);
#2041=EDGE_CURVE('',#1572,#1573,#989,.T.);
#2042=EDGE_CURVE('',#1573,#1573,#1348,.T.);
#2043=EDGE_CURVE('',#1574,#1574,#1349,.T.);
#2044=EDGE_CURVE('',#1574,#1575,#990,.T.);
#2045=EDGE_CURVE('',#1575,#1575,#1350,.T.);
#2901=ORIENTED_EDGE('',*,*,#2040,.F.);
#2902=ORIENTED_EDGE('',*,*,#2041,.T.);
#2903=ORIENTED_EDGE('',*,*,#2042,.T.);
#2904=ORIENTED_EDGE('',*,*,#2041,.F.);
#2905=ORIENTED_EDGE('',*,*,#2043,.F.);
#2906=ORIENTED_EDGE('',*,*,#2044,.T.);
#2907=ORIENTED_EDGE('',*,*,#2045,.T.);
#2908=ORIENTED_EDGE('',*,*,#2044,.F.);
#2909=ORIENTED_EDGE('',*,*,#2043,.T.);
#2910=ORIENTED_EDGE('',*,*,#2040,.T.);
#2911=ORIENTED_EDGE('',*,*,#2045,.F.);
#2912=ORIENTED_EDGE('',*,*,#2042,.F.);
#3427=CYLINDRICAL_SURFACE('',#3933,3.);
#3428=CYLINDRICAL_SURFACE('',#3936,6.);
#3611=ADVANCED_FACE('',(#535),#3427,.F.);
#3612=ADVANCED_FACE('',(#536),#3428,.T.);
#3613=ADVANCED_FACE('',(#537,#361),#403,.T.);
#3614=ADVANCED_FACE('',(#538,#362),#404,.F.);
#3697=CLOSED_SHELL('',(#3611,#3612,#3613,#3614));
#3932=AXIS2_PLACEMENT_3D('',#9380,#4516,#4517);
#3933=AXIS2_PLACEMENT_3D('',#9381,#4518,#4519);
#3934=AXIS2_PLACEMENT_3D('',#9383,#4520,#4521);
#3935=AXIS2_PLACEMENT_3D('',#9386,#4523,#4524);
#3936=AXIS2_PLACEMENT_3D('',#9387,#4525,#4526);
#3937=AXIS2_PLACEMENT_3D('',#9389,#4527,#4528);
#3938=AXIS2_PLACEMENT_3D('',#9392,#4530,#4531);
#3939=AXIS2_PLACEMENT_3D('',#9393,#4532,#4533);
#3940=AXIS2_PLACEMENT_3D('',#9394,#4534,#4535);
#4516=DIRECTION('axis',(0.,0.,1.));
#4517=DIRECTION('refdir',(1.,0.,0.));
#4518=DIRECTION('center_axis',(0.,0.,1.));
#4519=DIRECTION('ref_axis',(1.,0.,0.));
#4520=DIRECTION('center_axis',(0.,0.,-1.));
#4521=DIRECTION('ref_axis',(1.,0.,0.));
#4522=DIRECTION('',(0.,0.,-1.));
#4523=DIRECTION('center_axis',(0.,0.,-1.));
#4524=DIRECTION('ref_axis',(1.,0.,0.));
#4525=DIRECTION('center_axis',(0.,0.,1.));
#4526=DIRECTION('ref_axis',(1.,0.,0.));
#4527=DIRECTION('center_axis',(0.,0.,1.));
#4528=DIRECTION('ref_axis',(1.,0.,0.));
#4529=DIRECTION('',(0.,0.,-1.));
#4530=DIRECTION('center_axis',(0.,0.,1.));
#4531=DIRECTION('ref_axis',(1.,0.,0.));
#4532=DIRECTION('center_axis',(0.,0.,1.));
#4533=DIRECTION('ref_axis',(1.,0.,0.));
#4534=DIRECTION('center_axis',(0.,0.,1.));
#4535=DIRECTION('ref_axis',(1.,0.,0.));
#9380=CARTESIAN_POINT('',(0.,0.,0.));
#9381=CARTESIAN_POINT('Origin',(0.,0.,0.));
#9382=CARTESIAN_POINT('',(-3.,-3.67394039744206E-16,2.));
#9383=CARTESIAN_POINT('Origin',(0.,0.,2.));
#9384=CARTESIAN_POINT('',(-3.,-3.67394039744206E-16,0.));
#9385=CARTESIAN_POINT('',(-3.,-3.67394039744206E-16,0.));
#9386=CARTESIAN_POINT('Origin',(0.,0.,0.));
#9387=CARTESIAN_POINT('Origin',(0.,0.,0.));
#9388=CARTESIAN_POINT('',(-6.,-7.34788079488412E-16,2.));
#9389=CARTESIAN_POINT('Origin',(0.,0.,2.));
#9390=CARTESIAN_POINT('',(-6.,-7.34788079488412E-16,0.));
#9391=CARTESIAN_POINT('',(-6.,-7.34788079488412E-16,0.));
#9392=CARTESIAN_POINT('Origin',(0.,0.,0.));
#9393=CARTESIAN_POINT('Origin',(0.,0.,2.));
#9394=CARTESIAN_POINT('Origin',(0.,0.,0.));
#13789=UNCERTAINTY_MEASURE_WITH_UNIT(LENGTH_MEASURE(0.01),#13802,
'DISTANCE_ACCURACY_VALUE',
'Maximum model space distance between geometric entities at asserted c
onnectivities');
#13792=UNCERTAINTY_MEASURE_WITH_UNIT(LENGTH_MEASURE(0.01),#13802,
'DISTANCE_ACCURACY_VALUE',
'Maximum model space distance between geometric entities at asserted c
onnectivities');
#13798=(
GEOMETRIC_REPRESENTATION_CONTEXT(3)
GLOBAL_UNCERTAINTY_ASSIGNED_CONTEXT((#13789))
GLOBAL_UNIT_ASSIGNED_CONTEXT((#13802,#13804,#13805))
REPRESENTATION_CONTEXT('','3D')
);
#13801=(
GEOMETRIC_REPRESENTATION_CONTEXT(3)
GLOBAL_UNCERTAINTY_ASSIGNED_CONTEXT((#13792))
GLOBAL_UNIT_ASSIGNED_CONTEXT((#13802,#13804,#13805))
REPRESENTATION_CONTEXT('','3D')
);
#13802=(
LENGTH_UNIT()
NAMED_UNIT(*)
SI_UNIT(.MILLI.,.METRE.)
);
#13804=(
NAMED_UNIT(*)
PLANE_ANGLE_UNIT()
SI_UNIT($,.RADIAN.)
);
#13805=(
NAMED_UNIT(*)
SI_UNIT($,.STERADIAN.)
SOLID_ANGLE_UNIT()
);
#13811=SHAPE_DEFINITION_REPRESENTATION(#13819,#13838);
#13819=PRODUCT_DEFINITION_SHAPE('',$,#13847);
#13838=SHAPE_REPRESENTATION('',(#3932),#13798);
#13841=PRODUCT_DEFINITION_CONTEXT('part definition',#13867,'design');
#13847=PRODUCT_DEFINITION('Flat washer M5','Flat washer M5',#13855,#13841);
#13855=PRODUCT_DEFINITION_FORMATION('',$,#13874);
#13867=APPLICATION_CONTEXT(
'Core Data for Automotive Mechanical Design Process');
#13868=PRODUCT_CONTEXT('part definition',#13867,'mechanical');
#13874=PRODUCT('Flat washer M5','Flat washer M5',$,(#13868));
#13881=PRESENTATION_STYLE_ASSIGNMENT((#13888));
#13888=SURFACE_STYLE_USAGE(.BOTH.,#13895);
#13895=SURFACE_SIDE_STYLE('',(#13902));
#13902=SURFACE_STYLE_FILL_AREA(#13909);
#13909=FILL_AREA_STYLE('Light gray',(#13916));
#13916=FILL_AREA_STYLE_COLOUR('Light gray',#13923);
#13923=COLOUR_RGB('Light gray',0.725490196078431,0.752941176470588,0.792156862745098);
ENDSEC;
END-ISO-10303-21;
